ISO-10303-21;
HEADER;
/* Generated by software containing ST-Developer
 * from STEP Tools, Inc. (www.steptools.com) 
 */

FILE_DESCRIPTION(
/* description */ ('Fatigue rig crank-slider'),
/* implementation_level */ '2;1');

FILE_NAME(
/* name */ 'M5x14 Cap Screw.step',
/* time_stamp */ '2026-10-28T03:24:50-07:00',
/* author */ (''),
/* organization */ (''),
/* preprocessor_version */ 'ST-DEVELOPER v20.2',
/* originating_system */ 'Autodesk Translation Framework v15.17.0.0',
/* authorisation */ '');

FILE_SCHEMA (('AUTOMOTIVE_DESIGN { 1 0 10303 214 3 1 1 }'));
ENDSEC;

DATA;
#10=MECHANICAL_DESIGN_GEOMETRIC_PRESENTATION_REPRESENTATION('',(#642),#16911);
#26=CONICAL_SURFACE('',#10419,0.4,0.785398163397448);
#27=CONICAL_SURFACE('',#10423,0.41,0.785398163397448);
#28=CONICAL_SURFACE('',#10427,0.26,0.463647609000806);
#39=ORIENTED_CLOSED_SHELL('',*,#8935,.F.);
#44=BREP_WITH_VOIDS('Body1',#8936,(#39));
#533=SHAPE_REPRESENTATION_RELATIONSHIP('SRR','None',#17178,#583);
#583=ADVANCED_BREP_SHAPE_REPRESENTATION('',(#44),#16907);
#642=STYLED_ITEM('',(#17494),#44);
#892=FACE_BOUND('',#2415,.T.);
#1182=PLANE('',#10407);
#1183=PLANE('',#10408);
#1184=PLANE('',#10409);
#1185=PLANE('',#10410);
#1186=PLANE('',#10411);
#1187=PLANE('',#10412);
#1188=PLANE('',#10413);
#1189=PLANE('',#10414);
#1190=PLANE('',#10415);
#1191=PLANE('',#10417);
#1192=PLANE('',#10425);
#1686=FACE_OUTER_BOUND('',#2401,.T.);
#1687=FACE_OUTER_BOUND('',#2402,.T.);
#1688=FACE_OUTER_BOUND('',#2403,.T.);
#1689=FACE_OUTER_BOUND('',#2404,.T.);
#1690=FACE_OUTER_BOUND('',#2405,.T.);
#1691=FACE_OUTER_BOUND('',#2406,.T.);
#1692=FACE_OUTER_BOUND('',#2407,.T.);
#1693=FACE_OUTER_BOUND('',#2408,.T.);
#1694=FACE_OUTER_BOUND('',#2409,.T.);
#1695=FACE_OUTER_BOUND('',#2410,.T.);
#1696=FACE_OUTER_BOUND('',#2411,.T.);
#1697=FACE_OUTER_BOUND('',#2412,.T.);
#1698=FACE_OUTER_BOUND('',#2413,.T.);
#1699=FACE_OUTER_BOUND('',#2414,.T.);
#1700=FACE_OUTER_BOUND('',#2416,.T.);
#1701=FACE_OUTER_BOUND('',#2417,.T.);
#2401=EDGE_LOOP('',(#7996,#7997,#7998,#7999));
#2402=EDGE_LOOP('',(#8000,#8001,#8002,#8003));
#2403=EDGE_LOOP('',(#8004,#8005,#8006,#8007));
#2404=EDGE_LOOP('',(#8008,#8009,#8010,#8011));
#2405=EDGE_LOOP('',(#8012,#8013,#8014,#8015));
#2406=EDGE_LOOP('',(#8016,#8017,#8018,#8019));
#2407=EDGE_LOOP('',(#8020,#8021,#8022,#8023,#8024,#8025));
#2408=EDGE_LOOP('',(#8026,#8027,#8028,#8029,#8030,#8031));
#2409=EDGE_LOOP('',(#8032));
#2410=EDGE_LOOP('',(#8033));
#2411=EDGE_LOOP('',(#8034,#8035,#8036,#8037));
#2412=EDGE_LOOP('',(#8038,#8039,#8040,#8041));
#2413=EDGE_LOOP('',(#8042,#8043,#8044,#8045));
#2414=EDGE_LOOP('',(#8046));
#2415=EDGE_LOOP('',(#8047));
#2416=EDGE_LOOP('',(#8048,#8049,#8050,#8051));
#2417=EDGE_LOOP('',(#8052,#8053,#8054,#8055));
#3033=LINE('',#16502,#3679);
#3034=LINE('',#16504,#3680);
#3035=LINE('',#16506,#3681);
#3036=LINE('',#16507,#3682);
#3037=LINE('',#16510,#3683);
#3038=LINE('',#16512,#3684);
#3039=LINE('',#16513,#3685);
#3040=LINE('',#16516,#3686);
#3041=LINE('',#16518,#3687);
#3042=LINE('',#16519,#3688);
#3043=LINE('',#16522,#3689);
#3044=LINE('',#16524,#3690);
#3045=LINE('',#16525,#3691);
#3046=LINE('',#16528,#3692);
#3047=LINE('',#16530,#3693);
#3048=LINE('',#16531,#3694);
#3049=LINE('',#16533,#3695);
#3050=LINE('',#16534,#3696);
#3051=LINE('',#16546,#3697);
#3052=LINE('',#16550,#3698);
#3053=LINE('',#16554,#3699);
#3054=LINE('',#16561,#3700);
#3055=LINE('',#16563,#3701);
#3679=VECTOR('',#12969,1.);
#3680=VECTOR('',#12970,1.);
#3681=VECTOR('',#12971,1.);
#3682=VECTOR('',#12972,1.);
#3683=VECTOR('',#12975,1.);
#3684=VECTOR('',#12976,1.);
#3685=VECTOR('',#12977,1.);
#3686=VECTOR('',#12980,1.);
#3687=VECTOR('',#12981,1.);
#3688=VECTOR('',#12982,1.);
#3689=VECTOR('',#12985,1.);
#3690=VECTOR('',#12986,1.);
#3691=VECTOR('',#12987,1.);
#3692=VECTOR('',#12990,1.);
#3693=VECTOR('',#12991,1.);
#3694=VECTOR('',#12992,1.);
#3695=VECTOR('',#12995,1.);
#3696=VECTOR('',#12996,1.);
#3697=VECTOR('',#13013,0.4);
#3698=VECTOR('',#13018,0.425);
#3699=VECTOR('',#13023,0.41);
#3700=VECTOR('',#13032,0.26);
#3701=VECTOR('',#13035,0.25);
#4125=CIRCLE('',#10416,0.24505);
#4126=CIRCLE('',#10418,0.375);
#4127=CIRCLE('',#10420,0.425);
#4128=CIRCLE('',#10422,0.425);
#4129=CIRCLE('',#10424,0.395);
#4130=CIRCLE('',#10426,0.27);
#4131=CIRCLE('',#10428,0.24505);
#4833=VERTEX_POINT('',#16500);
#4834=VERTEX_POINT('',#16501);
#4835=VERTEX_POINT('',#16503);
#4836=VERTEX_POINT('',#16505);
#4837=VERTEX_POINT('',#16509);
#4838=VERTEX_POINT('',#16511);
#4839=VERTEX_POINT('',#16515);
#4840=VERTEX_POINT('',#16517);
#4841=VERTEX_POINT('',#16521);
#4842=VERTEX_POINT('',#16523);
#4843=VERTEX_POINT('',#16527);
#4844=VERTEX_POINT('',#16529);
#4845=VERTEX_POINT('',#16538);
#4846=VERTEX_POINT('',#16541);
#4847=VERTEX_POINT('',#16544);
#4848=VERTEX_POINT('',#16548);
#4849=VERTEX_POINT('',#16552);
#4850=VERTEX_POINT('',#16556);
#4851=VERTEX_POINT('',#16559);
#5896=EDGE_CURVE('',#4833,#4834,#3033,.T.);
#5897=EDGE_CURVE('',#4834,#4835,#3034,.T.);
#5898=EDGE_CURVE('',#4835,#4836,#3035,.T.);
#5899=EDGE_CURVE('',#4833,#4836,#3036,.T.);
#5900=EDGE_CURVE('',#4834,#4837,#3037,.T.);
#5901=EDGE_CURVE('',#4837,#4838,#3038,.T.);
#5902=EDGE_CURVE('',#4838,#4835,#3039,.T.);
#5903=EDGE_CURVE('',#4837,#4839,#3040,.T.);
#5904=EDGE_CURVE('',#4839,#4840,#3041,.T.);
#5905=EDGE_CURVE('',#4840,#4838,#3042,.T.);
#5906=EDGE_CURVE('',#4839,#4841,#3043,.T.);
#5907=EDGE_CURVE('',#4841,#4842,#3044,.T.);
#5908=EDGE_CURVE('',#4842,#4840,#3045,.T.);
#5909=EDGE_CURVE('',#4841,#4843,#3046,.T.);
#5910=EDGE_CURVE('',#4843,#4844,#3047,.T.);
#5911=EDGE_CURVE('',#4844,#4842,#3048,.T.);
#5912=EDGE_CURVE('',#4843,#4833,#3049,.T.);
#5913=EDGE_CURVE('',#4836,#4844,#3050,.T.);
#5914=EDGE_CURVE('',#4845,#4845,#4125,.T.);
#5915=EDGE_CURVE('',#4846,#4846,#4126,.T.);
#5916=EDGE_CURVE('',#4847,#4847,#4127,.T.);
#5917=EDGE_CURVE('',#4847,#4846,#3051,.T.);
#5918=EDGE_CURVE('',#4848,#4848,#4128,.T.);
#5919=EDGE_CURVE('',#4848,#4847,#3052,.T.);
#5920=EDGE_CURVE('',#4849,#4849,#4129,.T.);
#5921=EDGE_CURVE('',#4849,#4848,#3053,.T.);
#5922=EDGE_CURVE('',#4850,#4850,#4130,.T.);
#5923=EDGE_CURVE('',#4851,#4851,#4131,.F.);
#5924=EDGE_CURVE('',#4851,#4850,#3054,.T.);
#5925=EDGE_CURVE('',#4845,#4851,#3055,.T.);
#7996=ORIENTED_EDGE('',*,*,#5896,.T.);
#7997=ORIENTED_EDGE('',*,*,#5897,.T.);
#7998=ORIENTED_EDGE('',*,*,#5898,.T.);
#7999=ORIENTED_EDGE('',*,*,#5899,.F.);
#8000=ORIENTED_EDGE('',*,*,#5900,.T.);
#8001=ORIENTED_EDGE('',*,*,#5901,.T.);
#8002=ORIENTED_EDGE('',*,*,#5902,.T.);
#8003=ORIENTED_EDGE('',*,*,#5897,.F.);
#8004=ORIENTED_EDGE('',*,*,#5903,.T.);
#8005=ORIENTED_EDGE('',*,*,#5904,.T.);
#8006=ORIENTED_EDGE('',*,*,#5905,.T.);
#8007=ORIENTED_EDGE('',*,*,#5901,.F.);
#8008=ORIENTED_EDGE('',*,*,#5906,.T.);
#8009=ORIENTED_EDGE('',*,*,#5907,.T.);
#8010=ORIENTED_EDGE('',*,*,#5908,.T.);
#8011=ORIENTED_EDGE('',*,*,#5904,.F.);
#8012=ORIENTED_EDGE('',*,*,#5909,.T.);
#8013=ORIENTED_EDGE('',*,*,#5910,.T.);
#8014=ORIENTED_EDGE('',*,*,#5911,.T.);
#8015=ORIENTED_EDGE('',*,*,#5907,.F.);
#8016=ORIENTED_EDGE('',*,*,#5912,.T.);
#8017=ORIENTED_EDGE('',*,*,#5899,.T.);
#8018=ORIENTED_EDGE('',*,*,#5913,.T.);
#8019=ORIENTED_EDGE('',*,*,#5910,.F.);
#8020=ORIENTED_EDGE('',*,*,#5912,.F.);
#8021=ORIENTED_EDGE('',*,*,#5909,.F.);
#8022=ORIENTED_EDGE('',*,*,#5906,.F.);
#8023=ORIENTED_EDGE('',*,*,#5903,.F.);
#8024=ORIENTED_EDGE('',*,*,#5900,.F.);
#8025=ORIENTED_EDGE('',*,*,#5896,.F.);
#8026=ORIENTED_EDGE('',*,*,#5913,.F.);
#8027=ORIENTED_EDGE('',*,*,#5898,.F.);
#8028=ORIENTED_EDGE('',*,*,#5902,.F.);
#8029=ORIENTED_EDGE('',*,*,#5905,.F.);
#8030=ORIENTED_EDGE('',*,*,#5908,.F.);
#8031=ORIENTED_EDGE('',*,*,#5911,.F.);
#8032=ORIENTED_EDGE('',*,*,#5914,.F.);
#8033=ORIENTED_EDGE('',*,*,#5915,.F.);
#8034=ORIENTED_EDGE('',*,*,#5916,.F.);
#8035=ORIENTED_EDGE('',*,*,#5917,.T.);
#8036=ORIENTED_EDGE('',*,*,#5915,.T.);
#8037=ORIENTED_EDGE('',*,*,#5917,.F.);
#8038=ORIENTED_EDGE('',*,*,#5918,.F.);
#8039=ORIENTED_EDGE('',*,*,#5919,.T.);
#8040=ORIENTED_EDGE('',*,*,#5916,.T.);
#8041=ORIENTED_EDGE('',*,*,#5919,.F.);
#8042=ORIENTED_EDGE('',*,*,#5920,.F.);
#8043=ORIENTED_EDGE('',*,*,#5921,.T.);
#8044=ORIENTED_EDGE('',*,*,#5918,.T.);
#8045=ORIENTED_EDGE('',*,*,#5921,.F.);
#8046=ORIENTED_EDGE('',*,*,#5920,.T.);
#8047=ORIENTED_EDGE('',*,*,#5922,.F.);
#8048=ORIENTED_EDGE('',*,*,#5923,.F.);
#8049=ORIENTED_EDGE('',*,*,#5924,.T.);
#8050=ORIENTED_EDGE('',*,*,#5922,.T.);
#8051=ORIENTED_EDGE('',*,*,#5924,.F.);
#8052=ORIENTED_EDGE('',*,*,#5914,.T.);
#8053=ORIENTED_EDGE('',*,*,#5925,.T.);
#8054=ORIENTED_EDGE('',*,*,#5923,.T.);
#8055=ORIENTED_EDGE('',*,*,#5925,.F.);
#8347=CYLINDRICAL_SURFACE('',#10421,0.425);
#8348=CYLINDRICAL_SURFACE('',#10429,0.24505);
#8824=ADVANCED_FACE('',(#1686),#1182,.F.);
#8825=ADVANCED_FACE('',(#1687),#1183,.F.);
#8826=ADVANCED_FACE('',(#1688),#1184,.F.);
#8827=ADVANCED_FACE('',(#1689),#1185,.F.);
#8828=ADVANCED_FACE('',(#1690),#1186,.F.);
#8829=ADVANCED_FACE('',(#1691),#1187,.F.);
#8830=ADVANCED_FACE('',(#1692),#1188,.F.);
#8831=ADVANCED_FACE('',(#1693),#1189,.F.);
#8832=ADVANCED_FACE('',(#1694),#1190,.F.);
#8833=ADVANCED_FACE('',(#1695),#1191,.T.);
#8834=ADVANCED_FACE('',(#1696),#26,.T.);
#8835=ADVANCED_FACE('',(#1697),#8347,.T.);
#8836=ADVANCED_FACE('',(#1698),#27,.T.);
#8837=ADVANCED_FACE('',(#1699,#892),#1192,.T.);
#8838=ADVANCED_FACE('',(#1700),#28,.T.);
#8839=ADVANCED_FACE('',(#1701),#8348,.T.);
#8935=CLOSED_SHELL('',(#8824,#8825,#8826,#8827,#8828,#8829,#8830,#8831));
#8936=CLOSED_SHELL('',(#8832,#8833,#8834,#8835,#8836,#8837,#8838,#8839));
#10406=AXIS2_PLACEMENT_3D('',#16498,#12965,#12966);
#10407=AXIS2_PLACEMENT_3D('',#16499,#12967,#12968);
#10408=AXIS2_PLACEMENT_3D('',#16508,#12973,#12974);
#10409=AXIS2_PLACEMENT_3D('',#16514,#12978,#12979);
#10410=AXIS2_PLACEMENT_3D('',#16520,#12983,#12984);
#10411=AXIS2_PLACEMENT_3D('',#16526,#12988,#12989);
#10412=AXIS2_PLACEMENT_3D('',#16532,#12993,#12994);
#10413=AXIS2_PLACEMENT_3D('',#16535,#12997,#12998);
#10414=AXIS2_PLACEMENT_3D('',#16536,#12999,#13000);
#10415=AXIS2_PLACEMENT_3D('',#16537,#13001,#13002);
#10416=AXIS2_PLACEMENT_3D('',#16539,#13003,#13004);
#10417=AXIS2_PLACEMENT_3D('',#16540,#13005,#13006);
#10418=AXIS2_PLACEMENT_3D('',#16542,#13007,#13008);
#10419=AXIS2_PLACEMENT_3D('',#16543,#13009,#13010);
#10420=AXIS2_PLACEMENT_3D('',#16545,#13011,#13012);
#10421=AXIS2_PLACEMENT_3D('',#16547,#13014,#13015);
#10422=AXIS2_PLACEMENT_3D('',#16549,#13016,#13017);
#10423=AXIS2_PLACEMENT_3D('',#16551,#13019,#13020);
#10424=AXIS2_PLACEMENT_3D('',#16553,#13021,#13022);
#10425=AXIS2_PLACEMENT_3D('',#16555,#13024,#13025);
#10426=AXIS2_PLACEMENT_3D('',#16557,#13026,#13027);
#10427=AXIS2_PLACEMENT_3D('',#16558,#13028,#13029);
#10428=AXIS2_PLACEMENT_3D('',#16560,#13030,#13031);
#10429=AXIS2_PLACEMENT_3D('',#16562,#13033,#13034);
#12965=DIRECTION('axis',(0.,0.,1.));
#12966=DIRECTION('refdir',(1.,0.,0.));
#12967=DIRECTION('center_axis',(0.866025403784439,0.,-0.5));
#12968=DIRECTION('ref_axis',(0.5,0.,0.866025403784439));
#12969=DIRECTION('',(-0.5,0.,-0.866025403784439));
#12970=DIRECTION('',(0.,-1.,0.));
#12971=DIRECTION('',(0.5,0.,0.866025403784439));
#12972=DIRECTION('',(0.,-1.,0.));
#12973=DIRECTION('center_axis',(1.20185167898973E-16,0.,-1.));
#12974=DIRECTION('ref_axis',(1.,0.,1.20185167898973E-16));
#12975=DIRECTION('',(-1.,0.,-1.20185167898973E-16));
#12976=DIRECTION('',(0.,-1.,0.));
#12977=DIRECTION('',(1.,0.,1.20185167898973E-16));
#12978=DIRECTION('center_axis',(-0.866025403784439,0.,-0.5));
#12979=DIRECTION('ref_axis',(0.5,0.,-0.866025403784439));
#12980=DIRECTION('',(-0.5,0.,0.866025403784439));
#12981=DIRECTION('',(0.,-1.,0.));
#12982=DIRECTION('',(0.5,0.,-0.866025403784439));
#12983=DIRECTION('center_axis',(-0.866025403784439,0.,0.5));
#12984=DIRECTION('ref_axis',(-0.5,0.,-0.866025403784439));
#12985=DIRECTION('',(0.5,0.,0.866025403784439));
#12986=DIRECTION('',(0.,-1.,0.));
#12987=DIRECTION('',(-0.5,0.,-0.866025403784439));
#12988=DIRECTION('center_axis',(-2.40370335797945E-16,0.,1.));
#12989=DIRECTION('ref_axis',(-1.,0.,-2.40370335797945E-16));
#12990=DIRECTION('',(1.,0.,2.40370335797945E-16));
#12991=DIRECTION('',(0.,-1.,0.));
#12992=DIRECTION('',(-1.,0.,-2.40370335797945E-16));
#12993=DIRECTION('center_axis',(0.866025403784439,0.,0.5));
#12994=DIRECTION('ref_axis',(-0.5,0.,0.866025403784439));
#12995=DIRECTION('',(0.5,0.,-0.866025403784439));
#12996=DIRECTION('',(-0.5,0.,0.866025403784439));
#12997=DIRECTION('center_axis',(0.,1.,0.));
#12998=DIRECTION('ref_axis',(1.,0.,0.));
#12999=DIRECTION('center_axis',(0.,-1.,0.));
#13000=DIRECTION('ref_axis',(0.,0.,-1.));
#13001=DIRECTION('center_axis',(0.,1.,0.));
#13002=DIRECTION('ref_axis',(1.,0.,0.));
#13003=DIRECTION('center_axis',(0.,1.,0.));
#13004=DIRECTION('ref_axis',(1.,0.,0.));
#13005=DIRECTION('center_axis',(0.,1.,0.));
#13006=DIRECTION('ref_axis',(0.,0.,1.));
#13007=DIRECTION('center_axis',(0.,-1.,0.));
#13008=DIRECTION('ref_axis',(1.,0.,0.));
#13009=DIRECTION('center_axis',(0.,-1.,0.));
#13010=DIRECTION('ref_axis',(1.,0.,0.));
#13011=DIRECTION('center_axis',(0.,-1.,0.));
#13012=DIRECTION('ref_axis',(1.,0.,0.));
#13013=DIRECTION('',(0.707106781186548,0.707106781186547,8.65956056235493E-17));
#13014=DIRECTION('center_axis',(0.,-1.,0.));
#13015=DIRECTION('ref_axis',(1.,0.,0.));
#13016=DIRECTION('center_axis',(0.,-1.,0.));
#13017=DIRECTION('ref_axis',(1.,0.,0.));
#13018=DIRECTION('',(0.,1.,0.));
#13019=DIRECTION('center_axis',(0.,1.,0.));
#13020=DIRECTION('ref_axis',(1.,0.,0.));
#13021=DIRECTION('center_axis',(0.,-1.,0.));
#13022=DIRECTION('ref_axis',(1.,0.,0.));
#13023=DIRECTION('',(-0.707106781186547,0.707106781186548,-8.65956056235493E-17));
#13024=DIRECTION('center_axis',(0.,-1.,0.));
#13025=DIRECTION('ref_axis',(0.,0.,-1.));
#13026=DIRECTION('center_axis',(0.,-1.,0.));
#13027=DIRECTION('ref_axis',(1.,0.,0.));
#13028=DIRECTION('center_axis',(0.,1.,0.));
#13029=DIRECTION('ref_axis',(1.,0.,0.));
#13030=DIRECTION('center_axis',(0.,1.,0.));
#13031=DIRECTION('ref_axis',(1.,0.,0.));
#13032=DIRECTION('',(-0.447213595499958,0.894427190999916,-5.47678698264203E-17));
#13033=DIRECTION('center_axis',(0.,-1.,0.));
#13034=DIRECTION('ref_axis',(1.,0.,0.));
#13035=DIRECTION('',(0.,1.,0.));
#16498=CARTESIAN_POINT('',(0.,0.,0.));
#16499=CARTESIAN_POINT('Origin',(0.115470053837925,-0.5,-0.2));
#16500=CARTESIAN_POINT('',(0.23094010767585,-0.5,0.));
#16501=CARTESIAN_POINT('',(0.115470053837925,-0.5,-0.2));
#16502=CARTESIAN_POINT('',(0.23094010767585,-0.5,0.));
#16503=CARTESIAN_POINT('',(0.115470053837925,-0.8,-0.2));
#16504=CARTESIAN_POINT('',(0.115470053837925,-0.5,-0.2));
#16505=CARTESIAN_POINT('',(0.23094010767585,-0.8,0.));
#16506=CARTESIAN_POINT('',(0.23094010767585,-0.8,0.));
#16507=CARTESIAN_POINT('',(0.23094010767585,-0.5,0.));
#16508=CARTESIAN_POINT('Origin',(-0.115470053837925,-0.5,-0.2));
#16509=CARTESIAN_POINT('',(-0.115470053837925,-0.5,-0.2));
#16510=CARTESIAN_POINT('',(0.115470053837925,-0.5,-0.2));
#16511=CARTESIAN_POINT('',(-0.115470053837925,-0.8,-0.2));
#16512=CARTESIAN_POINT('',(-0.115470053837925,-0.5,-0.2));
#16513=CARTESIAN_POINT('',(0.115470053837925,-0.8,-0.2));
#16514=CARTESIAN_POINT('Origin',(-0.23094010767585,-0.5,-2.77555756156289E-17));
#16515=CARTESIAN_POINT('',(-0.23094010767585,-0.5,-2.82820063659975E-17));
#16516=CARTESIAN_POINT('',(-0.115470053837925,-0.5,-0.2));
#16517=CARTESIAN_POINT('',(-0.23094010767585,-0.8,-2.77555756156289E-17));
#16518=CARTESIAN_POINT('',(-0.23094010767585,-0.5,-2.82820063659975E-17));
#16519=CARTESIAN_POINT('',(-0.115470053837925,-0.8,-0.2));
#16520=CARTESIAN_POINT('Origin',(-0.115470053837925,-0.5,0.2));
#16521=CARTESIAN_POINT('',(-0.115470053837925,-0.5,0.2));
#16522=CARTESIAN_POINT('',(-0.23094010767585,-0.5,-2.82820063659975E-17));
#16523=CARTESIAN_POINT('',(-0.115470053837925,-0.8,0.2));
#16524=CARTESIAN_POINT('',(-0.115470053837925,-0.5,0.2));
#16525=CARTESIAN_POINT('',(-0.23094010767585,-0.8,-2.82820063659975E-17));
#16526=CARTESIAN_POINT('Origin',(0.115470053837925,-0.5,0.2));
#16527=CARTESIAN_POINT('',(0.115470053837925,-0.5,0.2));
#16528=CARTESIAN_POINT('',(-0.115470053837925,-0.5,0.2));
#16529=CARTESIAN_POINT('',(0.115470053837925,-0.8,0.2));
#16530=CARTESIAN_POINT('',(0.115470053837925,-0.5,0.2));
#16531=CARTESIAN_POINT('',(-0.115470053837925,-0.8,0.2));
#16532=CARTESIAN_POINT('Origin',(0.23094010767585,-0.5,0.));
#16533=CARTESIAN_POINT('',(0.115470053837925,-0.5,0.2));
#16534=CARTESIAN_POINT('',(0.115470053837925,-0.8,0.2));
#16535=CARTESIAN_POINT('Origin',(0.,-0.5,0.));
#16536=CARTESIAN_POINT('Origin',(0.,-0.8,0.));
#16537=CARTESIAN_POINT('Origin',(0.,-1.4,0.));
#16538=CARTESIAN_POINT('',(-0.24505,-1.4,3.00099698131059E-17));
#16539=CARTESIAN_POINT('Origin',(0.,-1.4,0.));
#16540=CARTESIAN_POINT('Origin',(0.375,0.5,0.));
#16541=CARTESIAN_POINT('',(-0.375,0.5,-4.59242549680257E-17));
#16542=CARTESIAN_POINT('Origin',(0.,0.5,0.));
#16543=CARTESIAN_POINT('Origin',(0.,0.475,0.));
#16544=CARTESIAN_POINT('',(-0.425,0.45,-5.20474889637625E-17));
#16545=CARTESIAN_POINT('Origin',(0.,0.45,0.));
#16546=CARTESIAN_POINT('',(-0.4,0.475,-4.89858719658941E-17));
#16547=CARTESIAN_POINT('Origin',(0.,0.24,0.));
#16548=CARTESIAN_POINT('',(-0.425,0.0299999999999998,-5.20474889637625E-17));
#16549=CARTESIAN_POINT('Origin',(0.,0.0299999999999998,0.));
#16550=CARTESIAN_POINT('',(-0.425,0.24,-5.20474889637625E-17));
#16551=CARTESIAN_POINT('Origin',(0.,0.0150000000000001,0.));
#16552=CARTESIAN_POINT('',(-0.395,4.85722573273506E-17,-4.83735485663204E-17));
#16553=CARTESIAN_POINT('Origin',(0.,0.,0.));
#16554=CARTESIAN_POINT('',(-0.41,0.0150000000000001,-5.02105187650415E-17));
#16555=CARTESIAN_POINT('Origin',(0.27,0.,0.));
#16556=CARTESIAN_POINT('',(-0.27,0.,-3.30654635769785E-17));
#16557=CARTESIAN_POINT('Origin',(0.,0.,0.));
#16558=CARTESIAN_POINT('Origin',(0.,-0.02,0.));
#16559=CARTESIAN_POINT('',(-0.24505,-0.0498999999999999,3.00099698131059E-17));
#16560=CARTESIAN_POINT('Origin',(0.,-0.0498999999999999,0.));
#16561=CARTESIAN_POINT('',(-0.26,-0.02,-3.18408167778312E-17));
#16562=CARTESIAN_POINT('Origin',(0.,-0.995,0.));
#16563=CARTESIAN_POINT('',(-0.24505,-0.995,-3.00099698131059E-17));
#16848=UNCERTAINTY_MEASURE_WITH_UNIT(LENGTH_MEASURE(0.001),#16912,
'DISTANCE_ACCURACY_VALUE',
'Maximum model space distance between geometric entities at asserted c
onnectivities');
#16852=UNCERTAINTY_MEASURE_WITH_UNIT(LENGTH_MEASURE(0.001),#16912,
'DISTANCE_ACCURACY_VALUE',
'Maximum model space distance between geometric entities at asserted c
onnectivities');
#16907=(
GEOMETRIC_REPRESENTATION_CONTEXT(3)
GLOBAL_UNCERTAINTY_ASSIGNED_CONTEXT((#16848))
GLOBAL_UNIT_ASSIGNED_CONTEXT((#16912,#16914,#16915))
REPRESENTATION_CONTEXT('','3D')
);
#16911=(
GEOMETRIC_REPRESENTATION_CONTEXT(3)
GLOBAL_UNCERTAINTY_ASSIGNED_CONTEXT((#16852))
GLOBAL_UNIT_ASSIGNED_CONTEXT((#16912,#16914,#16915))
REPRESENTATION_CONTEXT('','3D')
);
#16912=(
LENGTH_UNIT()
NAMED_UNIT(*)
SI_UNIT(.CENTI.,.METRE.)
);
#16914=(
NAMED_UNIT(*)
PLANE_ANGLE_UNIT()
SI_UNIT($,.RADIAN.)
);
#16915=(
NAMED_UNIT(*)
SI_UNIT($,.STERADIAN.)
SOLID_ANGLE_UNIT()
);
#16970=SHAPE_DEFINITION_REPRESENTATION(#17045,#17178);
#17045=PRODUCT_DEFINITION_SHAPE('',$,#17237);
#17178=SHAPE_REPRESENTATION('',(#10406),#16907);
#17182=PRODUCT_DEFINITION_CONTEXT('part definition',#17358,'design');
#17237=PRODUCT_DEFINITION('M5x14 Cap Screw','M5x14 Cap Screw',#17295,#17182);
#17295=PRODUCT_DEFINITION_FORMATION('',$,#17414);
#17358=APPLICATION_CONTEXT(
'Core Data for Automotive Mechanical Design Process');
#17359=PRODUCT_CONTEXT('part definition',#17358,'mechanical');
#17414=PRODUCT('M5x14 Cap Screw','M5x14 Cap Screw','M5x14 Cap Screw',(#17359));
#17488=COLOUR_RGB('Black',0.12,0.14,0.17);
#17489=FILL_AREA_STYLE_COLOUR('',#17488);
#17490=FILL_AREA_STYLE('',(#17489));
#17491=SURFACE_STYLE_FILL_AREA(#17490);
#17492=SURFACE_SIDE_STYLE('',(#17491));
#17493=SURFACE_STYLE_USAGE(.BOTH.,#17492);
#17494=PRESENTATION_STYLE_ASSIGNMENT((#17493));
ENDSEC;
END-ISO-10303-21;
